ISO-10303-21;
HEADER;
FILE_DESCRIPTION (('STEP AP214'),
    '1' );
FILE_NAME ('plain washer clevis pin grade a_iso_ISO 8738 - 8.step',
    '2026-10-08T05:56:58',
    ( '' ),
    ( '' ),
    'SwSTEP 2.0',
    'SolidWorks 2026',
    '' );
FILE_SCHEMA (( 'AUTOMOTIVE_DESIGN' ));
ENDSEC;

DATA;
#118=CARTESIAN_POINT ( 'NONE',  ( -34.92499999999994742, 0.000000000000000000, 4.000000000000000000 ) ) ;
#279=( GEOMETRIC_REPRESENTATION_CONTEXT ( 3 ) GLOBAL_UNCERTAINTY_ASSIGNED_CONTEXT ( ( #18002 ) ) GLOBAL_UNIT_ASSIGNED_CONTEXT ( ( #11074, #12777, #13979 ) ) REPRESENTATION_CONTEXT ( 'NONE', 'WORKASPACE' ) );
#307=VERTEX_POINT ( 'NONE', #8239 ) ;
#547=EDGE_CURVE ( 'NONE', #307, #4366, #2908, .T. ) ;
#923=DIRECTION ( 'NONE',  ( -1.000000000000000000, -0.000000000000000000, -0.000000000000000000 ) ) ;
#1118=ADVANCED_BREP_SHAPE_REPRESENTATION ( '', ( #16042, #16724 ), #279 ) ;
#1313=EDGE_LOOP ( 'NONE', ( #12513, #13833, #5318, #8910 ) ) ;
#1339=CARTESIAN_POINT ( 'NONE',  ( -34.92499999999994742, 9.184850993605147944E-16, -7.500000000000000000 ) ) ;
#1394=ORIENTED_EDGE ( 'NONE', *, *, #7977, .T. ) ;
#1444=CYLINDRICAL_SURFACE ( 'NONE', #5257, 7.500000000000000000 ) ;
#1928=DIRECTION ( 'NONE',  ( -1.000000000000000000, -0.000000000000000000, -0.000000000000000000 ) ) ;
#1968=CARTESIAN_POINT ( 'NONE',  ( 0.000000000000000000, 0.000000000000000000, 0.000000000000000000 ) ) ;
#2007=CARTESIAN_POINT ( 'NONE',  ( -2.000000000000001776, 0.000000000000000000, 0.000000000000000000 ) ) ;
#2077=VERTEX_POINT ( 'NONE', #5085 ) ;
#2153=EDGE_LOOP ( 'NONE', ( #16857, #17540, #2215, #19662 ) ) ;
#2215=ORIENTED_EDGE ( 'NONE', *, *, #547, .T. ) ;
#2224=PRODUCT_DEFINITION ( 'UNKNOWN', '', #19766, #17599 ) ;
#2380=CARTESIAN_POINT ( 'NONE',  ( 0.000000000000000000, 0.000000000000000000, 0.000000000000000000 ) ) ;
#2450=( NAMED_UNIT ( * ) PLANE_ANGLE_UNIT ( ) SI_UNIT ( $, .RADIAN. ) );
#2652=APPLICATION_CONTEXT ( 'automotive_design' ) ;
#2908=LINE ( 'NONE', #118, #4553 ) ;
#2985=DIRECTION ( 'NONE',  ( -1.000000000000000000, -0.000000000000000000, -0.000000000000000000 ) ) ;
#3033=VERTEX_POINT ( 'NONE', #7797 ) ;
#3078=CARTESIAN_POINT ( 'NONE',  ( -2.000000000000001776, 9.184850993605147944E-16, -7.500000000000000000 ) ) ;
#3182=DIRECTION ( 'NONE',  ( 0.000000000000000000, 0.000000000000000000, 1.000000000000000000 ) ) ;
#3239=CYLINDRICAL_SURFACE ( 'NONE', #13599, 4.000000000000000000 ) ;
#3241=CARTESIAN_POINT ( 'NONE',  ( -2.000000000000000888, 7.500000000000000000, 0.000000000000000000 ) ) ;
#3274=DIRECTION ( 'NONE',  ( 0.000000000000000000, 0.000000000000000000, 1.000000000000000000 ) ) ;
#3407=AXIS2_PLACEMENT_3D ( 'NONE', #2380, #14601, #6968 ) ;
#3624=PRODUCT ( 'plain washer clevis pin grade a_iso_ISO 8738 - 8', 'plain washer clevis pin grade a_iso_ISO 8738 - 8', '', ( #14153 ) ) ;
#3762=VECTOR ( 'NONE', #18432, 1000.000000000000000 ) ;
#3858=ORIENTED_EDGE ( 'NONE', *, *, #11932, .F. ) ;
#3861=( NAMED_UNIT ( * ) SI_UNIT ( $, .STERADIAN. ) SOLID_ANGLE_UNIT ( ) );
#3965=SURFACE_SIDE_STYLE ('',( #14484 ) ) ;
#3973=DIRECTION ( 'NONE',  ( -1.000000000000000000, -0.000000000000000000, -0.000000000000000000 ) ) ;
#4000=EDGE_LOOP ( 'NONE', ( #9435, #9994 ) ) ;
#4293=CARTESIAN_POINT ( 'NONE',  ( -2.000000000000001776, 0.000000000000000000, 7.500000000000000000 ) ) ;
#4343=DIRECTION ( 'NONE',  ( -1.000000000000000000, -0.000000000000000000, -0.000000000000000000 ) ) ;
#4348=CIRCLE ( 'NONE', #15540, 7.500000000000000000 ) ;
#4357=ORIENTED_EDGE ( 'NONE', *, *, #7956, .F. ) ;
#4366=VERTEX_POINT ( 'NONE', #13541 ) ;
#4553=VECTOR ( 'NONE', #18423, 1000.000000000000000 ) ;
#4652=SHAPE_REPRESENTATION ( 'plain washer clevis pin grade a_iso_ISO 8738 - 8', ( #16724 ), #279 ) ;
#4816=DIRECTION ( 'NONE',  ( -0.000000000000000000, 0.000000000000000000, 1.000000000000000000 ) ) ;
#4951=VERTEX_POINT ( 'NONE', #3078 ) ;
#5085=CARTESIAN_POINT ( 'NONE',  ( 0.000000000000000000, 9.184850993605147944E-16, -7.500000000000000000 ) ) ;
#5177=CARTESIAN_POINT ( 'NONE',  ( -2.000000000000001776, 0.000000000000000000, 0.000000000000000000 ) ) ;
#5227=DIRECTION ( 'NONE',  ( 0.000000000000000000, 0.000000000000000000, 1.000000000000000000 ) ) ;
#5257=AXIS2_PLACEMENT_3D ( 'NONE', #16951, #16557, #10746 ) ;
#5318=ORIENTED_EDGE ( 'NONE', *, *, #6103, .T. ) ;
#5390=( GEOMETRIC_REPRESENTATION_CONTEXT ( 3 ) GLOBAL_UNCERTAINTY_ASSIGNED_CONTEXT ( ( #10399 ) ) GLOBAL_UNIT_ASSIGNED_CONTEXT ( ( #8268, #2450, #3861 ) ) REPRESENTATION_CONTEXT ( 'NONE', 'WORKASPACE' ) );
#5468=VECTOR ( 'NONE', #4343, 1000.000000000000000 ) ;
#5470=EDGE_CURVE ( 'NONE', #3033, #2077, #13285, .T. ) ;
#5565=AXIS2_PLACEMENT_3D ( 'NONE', #3241, #6330, #17250 ) ;
#5833=LINE ( 'NONE', #1339, #5468 ) ;
#5847=( LENGTH_UNIT ( ) NAMED_UNIT ( * ) SI_UNIT ( .MILLI., .METRE. ) );
#5857=EDGE_CURVE ( 'NONE', #4951, #6213, #4348, .T. ) ;
#5928=ORIENTED_EDGE ( 'NONE', *, *, #11293, .T. ) ;
#5948=ORIENTED_EDGE ( 'NONE', *, *, #7977, .F. ) ;
#6044=SURFACE_SIDE_STYLE ('',( #10761 ) ) ;
#6103=EDGE_CURVE ( 'NONE', #13819, #4366, #12680, .T. ) ;
#6213=VERTEX_POINT ( 'NONE', #4293 ) ;
#6230=DIRECTION ( 'NONE',  ( 1.000000000000000000, 0.000000000000000000, 0.000000000000000000 ) ) ;
#6260=EDGE_LOOP ( 'NONE', ( #5928, #13945 ) ) ;
#6330=DIRECTION ( 'NONE',  ( 1.000000000000000000, 0.000000000000000000, 0.000000000000000000 ) ) ;
#6414=CIRCLE ( 'NONE', #7368, 4.000000000000000000 ) ;
#6693=PLANE ( 'NONE',  #9322 ) ;
#6749=SHAPE_REPRESENTATION_RELATIONSHIP ( 'NONE' , 'NONE' ,  #4652, #1118 ) ;
#6844=EDGE_CURVE ( 'NONE', #4366, #13819, #6414, .T. ) ;
#6903=AXIS2_PLACEMENT_3D ( 'NONE', #17875, #2985, #3182 ) ;
#6906=CARTESIAN_POINT ( 'NONE',  ( -2.000000000000001776, 0.000000000000000000, 0.000000000000000000 ) ) ;
#6946=SURFACE_STYLE_USAGE ( .BOTH. , #3965 ) ;
#6968=DIRECTION ( 'NONE',  ( 0.000000000000000000, 0.000000000000000000, 1.000000000000000000 ) ) ;
#7082=EDGE_LOOP ( 'NONE', ( #5948, #14096, #9498, #16301 ) ) ;
#7165=UNCERTAINTY_MEASURE_WITH_UNIT (LENGTH_MEASURE( 1.000000000000000082E-05 ), #5847, 'distance_accuracy_value', 'NONE');
#7310=AXIS2_PLACEMENT_3D ( 'NONE', #10252, #9871, #15958 ) ;
#7368=AXIS2_PLACEMENT_3D ( 'NONE', #6906, #923, #16031 ) ;
#7541=FILL_AREA_STYLE_COLOUR ( '', #16929 ) ;
#7646=SURFACE_STYLE_USAGE ( .BOTH. , #6044 ) ;
#7660=AXIS2_PLACEMENT_3D ( 'NONE', #7868, #15586, #3274 ) ;
#7797=CARTESIAN_POINT ( 'NONE',  ( 0.000000000000000000, 0.000000000000000000, 7.500000000000000000 ) ) ;
#7868=CARTESIAN_POINT ( 'NONE',  ( -34.92499999999994742, 0.000000000000000000, 0.000000000000000000 ) ) ;
#7956=EDGE_CURVE ( 'NONE', #2077, #3033, #14148, .T. ) ;
#7977=EDGE_CURVE ( 'NONE', #2077, #4951, #5833, .T. ) ;
#8004=FACE_BOUND ( 'NONE', #6260, .T. ) ;
#8121=CARTESIAN_POINT ( 'NONE',  ( -34.92499999999994742, 0.000000000000000000, 7.500000000000000000 ) ) ;
#8207=DIRECTION ( 'NONE',  ( 0.000000000000000000, 0.000000000000000000, 1.000000000000000000 ) ) ;
#8239=CARTESIAN_POINT ( 'NONE',  ( 0.000000000000000000, 0.000000000000000000, 4.000000000000000000 ) ) ;
#8263=CARTESIAN_POINT ( 'NONE',  ( -2.000000000000001776, 4.898587196589412829E-16, -4.000000000000000000 ) ) ;
#8268=( LENGTH_UNIT ( ) NAMED_UNIT ( * ) SI_UNIT ( .MILLI., .METRE. ) );
#8567=CARTESIAN_POINT ( 'NONE',  ( 0.000000000000000000, 4.898587196589412829E-16, -4.000000000000000000 ) ) ;
#8758=DIRECTION ( 'NONE',  ( -1.000000000000000000, -0.000000000000000000, -0.000000000000000000 ) ) ;
#8866=( NAMED_UNIT ( * ) SI_UNIT ( $, .STERADIAN. ) SOLID_ANGLE_UNIT ( ) );
#8910=ORIENTED_EDGE ( 'NONE', *, *, #547, .F. ) ;
#9322=AXIS2_PLACEMENT_3D ( 'NONE', #17319, #17125, #4816 ) ;
#9333=ADVANCED_FACE ( 'NONE', ( #19648 ), #1444, .T. ) ;
#9355=CARTESIAN_POINT ( 'NONE',  ( -34.92499999999994742, 0.000000000000000000, 0.000000000000000000 ) ) ;
#9435=ORIENTED_EDGE ( 'NONE', *, *, #6844, .F. ) ;
#9488=DIRECTION ( 'NONE',  ( 0.000000000000000000, 0.000000000000000000, 1.000000000000000000 ) ) ;
#9498=ORIENTED_EDGE ( 'NONE', *, *, #11932, .T. ) ;
#9553=CIRCLE ( 'NONE', #11770, 4.000000000000000000 ) ;
#9620=DIRECTION ( 'NONE',  ( -1.000000000000000000, -0.000000000000000000, -0.000000000000000000 ) ) ;
#9833=DIRECTION ( 'NONE',  ( 0.000000000000000000, 0.000000000000000000, 1.000000000000000000 ) ) ;
#9871=DIRECTION ( 'NONE',  ( -1.000000000000000000, -0.000000000000000000, -0.000000000000000000 ) ) ;
#9994=ORIENTED_EDGE ( 'NONE', *, *, #6103, .F. ) ;
#10171=FILL_AREA_STYLE_COLOUR ( '', #11158 ) ;
#10252=CARTESIAN_POINT ( 'NONE',  ( -34.92499999999994742, 0.000000000000000000, 0.000000000000000000 ) ) ;
#10366=LINE ( 'NONE', #19657, #13848 ) ;
#10399=UNCERTAINTY_MEASURE_WITH_UNIT (LENGTH_MEASURE( 1.000000000000000082E-05 ), #8268, 'distance_accuracy_value', 'NONE');
#10451=ADVANCED_FACE ( 'NONE', ( #18547 ), #3239, .F. ) ;
#10539=MECHANICAL_DESIGN_GEOMETRIC_PRESENTATION_REPRESENTATION('',(#13089),#15650);
#10594=AXIS2_PLACEMENT_3D ( 'NONE', #17679, #3973, #19740 ) ;
#10746=DIRECTION ( 'NONE',  ( 0.000000000000000000, 0.000000000000000000, 1.000000000000000000 ) ) ;
#10759=SHAPE_DEFINITION_REPRESENTATION ( #14983, #4652 ) ;
#10761=SURFACE_STYLE_FILL_AREA ( #18457 ) ;
#10846=ORIENTED_EDGE ( 'NONE', *, *, #19070, .F. ) ;
#11074=( LENGTH_UNIT ( ) NAMED_UNIT ( * ) SI_UNIT ( .MILLI., .METRE. ) );
#11153=FACE_OUTER_BOUND ( 'NONE', #17818, .T. ) ;
#11158=COLOUR_RGB ( '', 0.09019608, 0.27058824, 0.51372549) ;
#11227=LINE ( 'NONE', #8121, #3762 ) ;
#11293=EDGE_CURVE ( 'NONE', #307, #13120, #12032, .T. ) ;
#11296=DIRECTION ( 'NONE',  ( -1.000000000000000000, -0.000000000000000000, -0.000000000000000000 ) ) ;
#11469=STYLED_ITEM ( 'NONE', ( #19259 ), #1118 ) ;
#11594=CLOSED_SHELL ( 'NONE', ( #9333, #16263, #10451, #18464, #17123, #15041 ) ) ;
#11770=AXIS2_PLACEMENT_3D ( 'NONE', #1968, #17085, #9488 ) ;
#11932=EDGE_CURVE ( 'NONE', #3033, #6213, #11227, .T. ) ;
#12032=CIRCLE ( 'NONE', #3407, 4.000000000000000000 ) ;
#12240=CIRCLE ( 'NONE', #13496, 7.500000000000000000 ) ;
#12292=FACE_OUTER_BOUND ( 'NONE', #7082, .T. ) ;
#12513=ORIENTED_EDGE ( 'NONE', *, *, #12879, .F. ) ;
#12632=EDGE_LOOP ( 'NONE', ( #18071, #1394, #10846, #3858 ) ) ;
#12680=CIRCLE ( 'NONE', #6903, 4.000000000000000000 ) ;
#12777=( NAMED_UNIT ( * ) PLANE_ANGLE_UNIT ( ) SI_UNIT ( $, .RADIAN. ) );
#12879=EDGE_CURVE ( 'NONE', #13120, #307, #9553, .T. ) ;
#12974=FILL_AREA_STYLE ('',( #10171 ) ) ;
#13089=STYLED_ITEM ( 'NONE', ( #13664 ), #16042 ) ;
#13120=VERTEX_POINT ( 'NONE', #8567 ) ;
#13285=CIRCLE ( 'NONE', #15207, 7.500000000000000000 ) ;
#13496=AXIS2_PLACEMENT_3D ( 'NONE', #5177, #11296, #15991 ) ;
#13541=CARTESIAN_POINT ( 'NONE',  ( -2.000000000000001776, 0.000000000000000000, 4.000000000000000000 ) ) ;
#13599=AXIS2_PLACEMENT_3D ( 'NONE', #9355, #15754, #15458 ) ;
#13664=PRESENTATION_STYLE_ASSIGNMENT (( #7646 ) ) ;
#13819=VERTEX_POINT ( 'NONE', #8263 ) ;
#13833=ORIENTED_EDGE ( 'NONE', *, *, #19592, .T. ) ;
#13848=VECTOR ( 'NONE', #8758, 1000.000000000000000 ) ;
#13923=FACE_OUTER_BOUND ( 'NONE', #16428, .T. ) ;
#13945=ORIENTED_EDGE ( 'NONE', *, *, #12879, .T. ) ;
#13979=( NAMED_UNIT ( * ) SI_UNIT ( $, .STERADIAN. ) SOLID_ANGLE_UNIT ( ) );
#14096=ORIENTED_EDGE ( 'NONE', *, *, #7956, .T. ) ;
#14148=CIRCLE ( 'NONE', #10594, 7.500000000000000000 ) ;
#14153=PRODUCT_CONTEXT ( 'NONE', #2652, 'mechanical' ) ;
#14484=SURFACE_STYLE_FILL_AREA ( #12974 ) ;
#14601=DIRECTION ( 'NONE',  ( -1.000000000000000000, -0.000000000000000000, -0.000000000000000000 ) ) ;
#14983=PRODUCT_DEFINITION_SHAPE ( 'NONE', 'NONE',  #2224 ) ;
#15041=ADVANCED_FACE ( 'NONE', ( #18747, #11153 ), #16961, .F. ) ;
#15207=AXIS2_PLACEMENT_3D ( 'NONE', #15644, #1928, #5227 ) ;
#15458=DIRECTION ( 'NONE',  ( 0.000000000000000000, 0.000000000000000000, 1.000000000000000000 ) ) ;
#15540=AXIS2_PLACEMENT_3D ( 'NONE', #2007, #9620, #8207 ) ;
#15586=DIRECTION ( 'NONE',  ( -1.000000000000000000, -0.000000000000000000, -0.000000000000000000 ) ) ;
#15644=CARTESIAN_POINT ( 'NONE',  ( 0.000000000000000000, 0.000000000000000000, 0.000000000000000000 ) ) ;
#15650=( GEOMETRIC_REPRESENTATION_CONTEXT ( 3 ) GLOBAL_UNCERTAINTY_ASSIGNED_CONTEXT ( ( #7165 ) ) GLOBAL_UNIT_ASSIGNED_CONTEXT ( ( #5847, #16774, #8866 ) ) REPRESENTATION_CONTEXT ( 'NONE', 'WORKASPACE' ) );
#15754=DIRECTION ( 'NONE',  ( -1.000000000000000000, -0.000000000000000000, -0.000000000000000000 ) ) ;
#15910=ORIENTED_EDGE ( 'NONE', *, *, #19070, .T. ) ;
#15958=DIRECTION ( 'NONE',  ( 0.000000000000000000, 0.000000000000000000, 1.000000000000000000 ) ) ;
#15991=DIRECTION ( 'NONE',  ( 0.000000000000000000, 0.000000000000000000, 1.000000000000000000 ) ) ;
#16031=DIRECTION ( 'NONE',  ( 0.000000000000000000, 0.000000000000000000, 1.000000000000000000 ) ) ;
#16042=MANIFOLD_SOLID_BREP ( 'Base-Revolve', #11594 ) ;
#16057=CYLINDRICAL_SURFACE ( 'NONE', #7310, 4.000000000000000000 ) ;
#16263=ADVANCED_FACE ( 'NONE', ( #17845 ), #16057, .F. ) ;
#16301=ORIENTED_EDGE ( 'NONE', *, *, #5857, .F. ) ;
#16428=EDGE_LOOP ( 'NONE', ( #19593, #4357 ) ) ;
#16557=DIRECTION ( 'NONE',  ( -1.000000000000000000, -0.000000000000000000, -0.000000000000000000 ) ) ;
#16724=AXIS2_PLACEMENT_3D ( 'NONE', #17428, #9833, #6230 ) ;
#16774=( NAMED_UNIT ( * ) PLANE_ANGLE_UNIT ( ) SI_UNIT ( $, .RADIAN. ) );
#16857=ORIENTED_EDGE ( 'NONE', *, *, #19592, .F. ) ;
#16929=COLOUR_RGB ( '', 0.09019608, 0.27058824, 0.51372549) ;
#16951=CARTESIAN_POINT ( 'NONE',  ( -34.92499999999994742, 0.000000000000000000, 0.000000000000000000 ) ) ;
#16961=PLANE ( 'NONE',  #5565 ) ;
#17085=DIRECTION ( 'NONE',  ( -1.000000000000000000, -0.000000000000000000, -0.000000000000000000 ) ) ;
#17123=ADVANCED_FACE ( 'NONE', ( #12292 ), #18388, .T. ) ;
#17125=DIRECTION ( 'NONE',  ( -1.000000000000000000, 0.000000000000000000, -0.000000000000000000 ) ) ;
#17250=DIRECTION ( 'NONE',  ( 0.000000000000000000, 0.000000000000000000, -1.000000000000000000 ) ) ;
#17319=CARTESIAN_POINT ( 'NONE',  ( 0.000000000000000000, 4.000000000000000000, 0.000000000000000000 ) ) ;
#17428=CARTESIAN_POINT ( 'NONE',  ( 0.000000000000000000, 0.000000000000000000, 0.000000000000000000 ) ) ;
#17540=ORIENTED_EDGE ( 'NONE', *, *, #11293, .F. ) ;
#17556=MECHANICAL_DESIGN_GEOMETRIC_PRESENTATION_REPRESENTATION('',(#11469),#5390);
#17599=PRODUCT_DEFINITION_CONTEXT ( 'detailed design', #18010, 'design' ) ;
#17679=CARTESIAN_POINT ( 'NONE',  ( 0.000000000000000000, 0.000000000000000000, 0.000000000000000000 ) ) ;
#17818=EDGE_LOOP ( 'NONE', ( #15910, #18985 ) ) ;
#17845=FACE_OUTER_BOUND ( 'NONE', #1313, .T. ) ;
#17875=CARTESIAN_POINT ( 'NONE',  ( -2.000000000000001776, 0.000000000000000000, 0.000000000000000000 ) ) ;
#18002=UNCERTAINTY_MEASURE_WITH_UNIT (LENGTH_MEASURE( 1.000000000000000082E-05 ), #11074, 'distance_accuracy_value', 'NONE');
#18010=APPLICATION_CONTEXT ( 'automotive_design' ) ;
#18071=ORIENTED_EDGE ( 'NONE', *, *, #5470, .T. ) ;
#18388=CYLINDRICAL_SURFACE ( 'NONE', #7660, 7.500000000000000000 ) ;
#18423=DIRECTION ( 'NONE',  ( -1.000000000000000000, -0.000000000000000000, -0.000000000000000000 ) ) ;
#18432=DIRECTION ( 'NONE',  ( -1.000000000000000000, -0.000000000000000000, -0.000000000000000000 ) ) ;
#18457=FILL_AREA_STYLE ('',( #7541 ) ) ;
#18464=ADVANCED_FACE ( 'NONE', ( #13923, #8004 ), #6693, .F. ) ;
#18547=FACE_OUTER_BOUND ( 'NONE', #2153, .T. ) ;
#18747=FACE_BOUND ( 'NONE', #4000, .T. ) ;
#18985=ORIENTED_EDGE ( 'NONE', *, *, #5857, .T. ) ;
#19070=EDGE_CURVE ( 'NONE', #6213, #4951, #12240, .T. ) ;
#19259=PRESENTATION_STYLE_ASSIGNMENT (( #6946 ) ) ;
#19592=EDGE_CURVE ( 'NONE', #13120, #13819, #10366, .T. ) ;
#19593=ORIENTED_EDGE ( 'NONE', *, *, #5470, .F. ) ;
#19648=FACE_OUTER_BOUND ( 'NONE', #12632, .T. ) ;
#19657=CARTESIAN_POINT ( 'NONE',  ( -34.92499999999994742, 4.898587196589412829E-16, -4.000000000000000000 ) ) ;
#19662=ORIENTED_EDGE ( 'NONE', *, *, #6844, .T. ) ;
#19740=DIRECTION ( 'NONE',  ( 0.000000000000000000, 0.000000000000000000, 1.000000000000000000 ) ) ;
#19766=PRODUCT_DEFINITION_FORMATION_WITH_SPECIFIED_SOURCE ( 'ANY', '', #3624, .NOT_KNOWN. ) ;
ENDSEC;
END-ISO-10303-21;
